ISO-10303-21;
HEADER;
/* Generated by software containing ST-Developer
 * from STEP Tools, Inc. (www.steptools.com) 
 */

FILE_DESCRIPTION(
/* description */ ('PAT-091'),
/* implementation_level */ '2;1');

FILE_NAME(
/* name */ 'Axle distance sleeve 5 mm (6).step',
/* time_stamp */ '2026-10-27T15:34:44-07:00',
/* author */ (''),
/* organization */ (''),
/* preprocessor_version */ 'ST-DEVELOPER v20.2',
/* originating_system */ 'Autodesk Translation Framework v15.17.0.0',
/* authorisation */ '');

FILE_SCHEMA (('AUTOMOTIVE_DESIGN { 1 0 10303 214 3 1 1 }'));
ENDSEC;

DATA;
#10=MECHANICAL_DESIGN_GEOMETRIC_PRESENTATION_REPRESENTATION('',(#1012),#25100);
#792=SHAPE_REPRESENTATION_RELATIONSHIP('SRR','None',#25555,#902);
#902=ADVANCED_BREP_SHAPE_REPRESENTATION('',(#1134),#25025);
#1012=STYLED_ITEM('',(#26191),#1134);
#1134=MANIFOLD_SOLID_BREP('Body1',#13291);
#1430=FACE_BOUND('',#3431,.T.);
#1431=FACE_BOUND('',#3433,.T.);
#1821=PLANE('',#15266);
#1822=PLANE('',#15267);
#2395=FACE_OUTER_BOUND('',#3428,.T.);
#2396=FACE_OUTER_BOUND('',#3429,.T.);
#2397=FACE_OUTER_BOUND('',#3430,.T.);
#2398=FACE_OUTER_BOUND('',#3432,.T.);
#3428=EDGE_LOOP('',(#10332,#10333,#10334,#10335));
#3429=EDGE_LOOP('',(#10336,#10337,#10338,#10339));
#3430=EDGE_LOOP('',(#10340));
#3431=EDGE_LOOP('',(#10341));
#3432=EDGE_LOOP('',(#10342));
#3433=EDGE_LOOP('',(#10343));
#4505=LINE('',#22513,#5245);
#4506=LINE('',#22519,#5246);
#5245=VECTOR('',#18203,0.604999999999997);
#5246=VECTOR('',#18210,0.799999999999997);
#5901=CIRCLE('',#15261,0.604999999999997);
#5902=CIRCLE('',#15262,0.604999999999997);
#5903=CIRCLE('',#15264,0.799999999999997);
#5904=CIRCLE('',#15265,0.799999999999997);
#6834=VERTEX_POINT('',#22510);
#6835=VERTEX_POINT('',#22512);
#6836=VERTEX_POINT('',#22516);
#6837=VERTEX_POINT('',#22518);
#8101=EDGE_CURVE('',#6834,#6834,#5901,.T.);
#8102=EDGE_CURVE('',#6834,#6835,#4505,.T.);
#8103=EDGE_CURVE('',#6835,#6835,#5902,.T.);
#8104=EDGE_CURVE('',#6836,#6836,#5903,.T.);
#8105=EDGE_CURVE('',#6836,#6837,#4506,.T.);
#8106=EDGE_CURVE('',#6837,#6837,#5904,.T.);
#10332=ORIENTED_EDGE('',*,*,#8101,.F.);
#10333=ORIENTED_EDGE('',*,*,#8102,.T.);
#10334=ORIENTED_EDGE('',*,*,#8103,.T.);
#10335=ORIENTED_EDGE('',*,*,#8102,.F.);
#10336=ORIENTED_EDGE('',*,*,#8104,.F.);
#10337=ORIENTED_EDGE('',*,*,#8105,.T.);
#10338=ORIENTED_EDGE('',*,*,#8106,.T.);
#10339=ORIENTED_EDGE('',*,*,#8105,.F.);
#10340=ORIENTED_EDGE('',*,*,#8104,.T.);
#10341=ORIENTED_EDGE('',*,*,#8101,.T.);
#10342=ORIENTED_EDGE('',*,*,#8106,.F.);
#10343=ORIENTED_EDGE('',*,*,#8103,.F.);
#12218=CYLINDRICAL_SURFACE('',#15260,0.604999999999997);
#12219=CYLINDRICAL_SURFACE('',#15263,0.799999999999997);
#12762=ADVANCED_FACE('',(#2395),#12218,.F.);
#12763=ADVANCED_FACE('',(#2396),#12219,.T.);
#12764=ADVANCED_FACE('',(#2397,#1430),#1821,.T.);
#12765=ADVANCED_FACE('',(#2398,#1431),#1822,.F.);
#13291=CLOSED_SHELL('',(#12762,#12763,#12764,#12765));
#15259=AXIS2_PLACEMENT_3D('',#22508,#18197,#18198);
#15260=AXIS2_PLACEMENT_3D('',#22509,#18199,#18200);
#15261=AXIS2_PLACEMENT_3D('',#22511,#18201,#18202);
#15262=AXIS2_PLACEMENT_3D('',#22514,#18204,#18205);
#15263=AXIS2_PLACEMENT_3D('',#22515,#18206,#18207);
#15264=AXIS2_PLACEMENT_3D('',#22517,#18208,#18209);
#15265=AXIS2_PLACEMENT_3D('',#22520,#18211,#18212);
#15266=AXIS2_PLACEMENT_3D('',#22521,#18213,#18214);
#15267=AXIS2_PLACEMENT_3D('',#22522,#18215,#18216);
#18197=DIRECTION('axis',(0.,0.,1.));
#18198=DIRECTION('refdir',(1.,0.,0.));
#18199=DIRECTION('center_axis',(0.,1.,0.));
#18200=DIRECTION('ref_axis',(1.,0.,0.));
#18201=DIRECTION('center_axis',(0.,-1.,0.));
#18202=DIRECTION('ref_axis',(1.,0.,0.));
#18203=DIRECTION('',(0.,-1.,0.));
#18204=DIRECTION('center_axis',(0.,-1.,0.));
#18205=DIRECTION('ref_axis',(1.,0.,0.));
#18206=DIRECTION('center_axis',(0.,1.,0.));
#18207=DIRECTION('ref_axis',(1.,0.,0.));
#18208=DIRECTION('center_axis',(0.,1.,0.));
#18209=DIRECTION('ref_axis',(1.,0.,0.));
#18210=DIRECTION('',(0.,-1.,0.));
#18211=DIRECTION('center_axis',(0.,1.,0.));
#18212=DIRECTION('ref_axis',(1.,0.,0.));
#18213=DIRECTION('center_axis',(0.,1.,0.));
#18214=DIRECTION('ref_axis',(1.,0.,0.));
#18215=DIRECTION('center_axis',(0.,1.,0.));
#18216=DIRECTION('ref_axis',(1.,0.,0.));
#22508=CARTESIAN_POINT('',(0.,0.,0.));
#22509=CARTESIAN_POINT('Origin',(38.7298334620742,8.,3.));
#22510=CARTESIAN_POINT('',(38.1248334620742,8.5,3.));
#22511=CARTESIAN_POINT('Origin',(38.7298334620742,8.5,3.));
#22512=CARTESIAN_POINT('',(38.1248334620742,8.,3.));
#22513=CARTESIAN_POINT('',(38.1248334620742,8.,3.));
#22514=CARTESIAN_POINT('Origin',(38.7298334620742,8.,3.));
#22515=CARTESIAN_POINT('Origin',(38.7298334620742,8.,3.));
#22516=CARTESIAN_POINT('',(37.9298334620742,8.5,3.));
#22517=CARTESIAN_POINT('Origin',(38.7298334620742,8.5,3.));
#22518=CARTESIAN_POINT('',(37.9298334620742,8.,3.));
#22519=CARTESIAN_POINT('',(37.9298334620742,8.,3.));
#22520=CARTESIAN_POINT('Origin',(38.7298334620742,8.,3.));
#22521=CARTESIAN_POINT('Origin',(38.7298334620742,8.5,3.));
#22522=CARTESIAN_POINT('Origin',(38.7298334620742,8.,3.));
#24904=UNCERTAINTY_MEASURE_WITH_UNIT(LENGTH_MEASURE(0.001),#25101,
'DISTANCE_ACCURACY_VALUE',
'Maximum model space distance between geometric entities at asserted c
onnectivities');
#24979=UNCERTAINTY_MEASURE_WITH_UNIT(LENGTH_MEASURE(0.001),#25101,
'DISTANCE_ACCURACY_VALUE',
'Maximum model space distance between geometric entities at asserted c
onnectivities');
#25025=(
GEOMETRIC_REPRESENTATION_CONTEXT(3)
GLOBAL_UNCERTAINTY_ASSIGNED_CONTEXT((#24904))
GLOBAL_UNIT_ASSIGNED_CONTEXT((#25101,#25103,#25104))
REPRESENTATION_CONTEXT('','3D')
);
#25100=(
GEOMETRIC_REPRESENTATION_CONTEXT(3)
GLOBAL_UNCERTAINTY_ASSIGNED_CONTEXT((#24979))
GLOBAL_UNIT_ASSIGNED_CONTEXT((#25101,#25103,#25104))
REPRESENTATION_CONTEXT('','3D')
);
#25101=(
LENGTH_UNIT()
NAMED_UNIT(*)
SI_UNIT(.CENTI.,.METRE.)
);
#25103=(
NAMED_UNIT(*)
PLANE_ANGLE_UNIT()
SI_UNIT($,.RADIAN.)
);
#25104=(
NAMED_UNIT(*)
SI_UNIT($,.STERADIAN.)
SOLID_ANGLE_UNIT()
);
#25150=SHAPE_DEFINITION_REPRESENTATION(#25270,#25555);
#25270=PRODUCT_DEFINITION_SHAPE('',$,#25676);
#25555=SHAPE_REPRESENTATION('',(#15259),#25025);
#25630=PRODUCT_DEFINITION_CONTEXT('part definition',#25992,'design');
#25676=PRODUCT_DEFINITION('Axle distance sleeve 5 mm (6)',
'Axle distance sleeve 5 mm (6)',#25796,#25630);
#25796=PRODUCT_DEFINITION_FORMATION('',$,#26039);
#25992=APPLICATION_CONTEXT(
'Core Data for Automotive Mechanical Design Process');
#25993=PRODUCT_CONTEXT('part definition',#25992,'mechanical');
#26039=PRODUCT('Axle distance sleeve 5 mm (6)',
'Axle distance sleeve 5 mm (6)','Axle distance sleeve 5 mm (6)',(#25993));
#26185=COLOUR_RGB('Grey',0.48,0.52,0.57);
#26186=FILL_AREA_STYLE_COLOUR('',#26185);
#26187=FILL_AREA_STYLE('',(#26186));
#26188=SURFACE_STYLE_FILL_AREA(#26187);
#26189=SURFACE_SIDE_STYLE('',(#26188));
#26190=SURFACE_STYLE_USAGE(.BOTH.,#26189);
#26191=PRESENTATION_STYLE_ASSIGNMENT((#26190));
ENDSEC;
END-ISO-10303-21;
